ISO-10303-21;
HEADER;
/* Generated by software containing ST-Developer
 * from STEP Tools, Inc. (www.steptools.com) 
 */

FILE_DESCRIPTION(
/* description */ ('PAT-099'),
/* implementation_level */ '2;1');

FILE_NAME(
/* name */ 'M4x4 collar screw.step',
/* time_stamp */ '2026-10-29T17:25:42-07:00',
/* author */ (''),
/* organization */ (''),
/* preprocessor_version */ 'ST-DEVELOPER v20.2',
/* originating_system */ 'Autodesk Translation Framework v15.17.0.0',
/* authorisation */ '');

FILE_SCHEMA (('AUTOMOTIVE_DESIGN { 1 0 10303 214 3 1 1 }'));
ENDSEC;

DATA;
#10=MECHANICAL_DESIGN_GEOMETRIC_PRESENTATION_REPRESENTATION('',(#350),#11035);
#32=CONICAL_SURFACE('',#5389,0.185,0.785398163397449);
#300=SHAPE_REPRESENTATION_RELATIONSHIP('SRR','None',#11170,#325);
#325=ADVANCED_BREP_SHAPE_REPRESENTATION('',(#382),#11020);
#350=STYLED_ITEM('',(#11393),#382);
#382=MANIFOLD_SOLID_BREP('Body1',#4719);
#499=FACE_BOUND('',#1213,.T.);
#601=PLANE('',#5378);
#602=PLANE('',#5380);
#603=PLANE('',#5381);
#604=PLANE('',#5382);
#605=PLANE('',#5383);
#606=PLANE('',#5384);
#607=PLANE('',#5385);
#608=PLANE('',#5386);
#609=PLANE('',#5387);
#825=FACE_OUTER_BOUND('',#1204,.T.);
#826=FACE_OUTER_BOUND('',#1205,.T.);
#827=FACE_OUTER_BOUND('',#1206,.T.);
#828=FACE_OUTER_BOUND('',#1207,.T.);
#829=FACE_OUTER_BOUND('',#1208,.T.);
#830=FACE_OUTER_BOUND('',#1209,.T.);
#831=FACE_OUTER_BOUND('',#1210,.T.);
#832=FACE_OUTER_BOUND('',#1211,.T.);
#833=FACE_OUTER_BOUND('',#1212,.T.);
#834=FACE_OUTER_BOUND('',#1214,.T.);
#835=FACE_OUTER_BOUND('',#1215,.T.);
#1204=EDGE_LOOP('',(#3847));
#1205=EDGE_LOOP('',(#3848,#3849,#3850,#3851));
#1206=EDGE_LOOP('',(#3852,#3853,#3854,#3855));
#1207=EDGE_LOOP('',(#3856,#3857,#3858,#3859));
#1208=EDGE_LOOP('',(#3860,#3861,#3862,#3863));
#1209=EDGE_LOOP('',(#3864,#3865,#3866,#3867));
#1210=EDGE_LOOP('',(#3868,#3869,#3870,#3871));
#1211=EDGE_LOOP('',(#3872,#3873,#3874,#3875,#3876,#3877));
#1212=EDGE_LOOP('',(#3878));
#1213=EDGE_LOOP('',(#3879,#3880,#3881,#3882,#3883,#3884));
#1214=EDGE_LOOP('',(#3885,#3886,#3887,#3888));
#1215=EDGE_LOOP('',(#3889,#3890,#3891,#3892));
#1496=LINE('',#10069,#1748);
#1497=LINE('',#10071,#1749);
#1498=LINE('',#10073,#1750);
#1499=LINE('',#10074,#1751);
#1500=LINE('',#10077,#1752);
#1501=LINE('',#10079,#1753);
#1502=LINE('',#10080,#1754);
#1503=LINE('',#10083,#1755);
#1504=LINE('',#10085,#1756);
#1505=LINE('',#10086,#1757);
#1506=LINE('',#10089,#1758);
#1507=LINE('',#10091,#1759);
#1508=LINE('',#10092,#1760);
#1509=LINE('',#10095,#1761);
#1510=LINE('',#10097,#1762);
#1511=LINE('',#10098,#1763);
#1512=LINE('',#10100,#1764);
#1513=LINE('',#10101,#1765);
#1514=LINE('',#10109,#1766);
#1515=LINE('',#10111,#1767);
#1748=VECTOR('',#6551,1.);
#1749=VECTOR('',#6552,1.);
#1750=VECTOR('',#6553,1.);
#1751=VECTOR('',#6554,1.);
#1752=VECTOR('',#6557,1.);
#1753=VECTOR('',#6558,1.);
#1754=VECTOR('',#6559,1.);
#1755=VECTOR('',#6562,1.);
#1756=VECTOR('',#6563,1.);
#1757=VECTOR('',#6564,1.);
#1758=VECTOR('',#6567,1.);
#1759=VECTOR('',#6568,1.);
#1760=VECTOR('',#6569,1.);
#1761=VECTOR('',#6572,1.);
#1762=VECTOR('',#6573,1.);
#1763=VECTOR('',#6574,1.);
#1764=VECTOR('',#6577,1.);
#1765=VECTOR('',#6578,1.);
#1766=VECTOR('',#6589,0.185);
#1767=VECTOR('',#6592,0.2);
#2024=CIRCLE('',#5379,0.1954);
#2025=CIRCLE('',#5388,0.17);
#2026=CIRCLE('',#5390,0.1954);
#2380=VERTEX_POINT('',#10064);
#2381=VERTEX_POINT('',#10067);
#2382=VERTEX_POINT('',#10068);
#2383=VERTEX_POINT('',#10070);
#2384=VERTEX_POINT('',#10072);
#2385=VERTEX_POINT('',#10076);
#2386=VERTEX_POINT('',#10078);
#2387=VERTEX_POINT('',#10082);
#2388=VERTEX_POINT('',#10084);
#2389=VERTEX_POINT('',#10088);
#2390=VERTEX_POINT('',#10090);
#2391=VERTEX_POINT('',#10094);
#2392=VERTEX_POINT('',#10096);
#2393=VERTEX_POINT('',#10104);
#2394=VERTEX_POINT('',#10107);
#2900=EDGE_CURVE('',#2380,#2380,#2024,.T.);
#2901=EDGE_CURVE('',#2381,#2382,#1496,.T.);
#2902=EDGE_CURVE('',#2381,#2383,#1497,.T.);
#2903=EDGE_CURVE('',#2383,#2384,#1498,.T.);
#2904=EDGE_CURVE('',#2382,#2384,#1499,.T.);
#2905=EDGE_CURVE('',#2385,#2381,#1500,.T.);
#2906=EDGE_CURVE('',#2385,#2386,#1501,.T.);
#2907=EDGE_CURVE('',#2386,#2383,#1502,.T.);
#2908=EDGE_CURVE('',#2387,#2385,#1503,.T.);
#2909=EDGE_CURVE('',#2387,#2388,#1504,.T.);
#2910=EDGE_CURVE('',#2388,#2386,#1505,.T.);
#2911=EDGE_CURVE('',#2389,#2387,#1506,.T.);
#2912=EDGE_CURVE('',#2389,#2390,#1507,.T.);
#2913=EDGE_CURVE('',#2390,#2388,#1508,.T.);
#2914=EDGE_CURVE('',#2391,#2389,#1509,.T.);
#2915=EDGE_CURVE('',#2391,#2392,#1510,.T.);
#2916=EDGE_CURVE('',#2392,#2390,#1511,.T.);
#2917=EDGE_CURVE('',#2382,#2391,#1512,.T.);
#2918=EDGE_CURVE('',#2384,#2392,#1513,.T.);
#2919=EDGE_CURVE('',#2393,#2393,#2025,.T.);
#2920=EDGE_CURVE('',#2394,#2394,#2026,.T.);
#2921=EDGE_CURVE('',#2394,#2393,#1514,.T.);
#2922=EDGE_CURVE('',#2380,#2394,#1515,.T.);
#3847=ORIENTED_EDGE('',*,*,#2900,.F.);
#3848=ORIENTED_EDGE('',*,*,#2901,.F.);
#3849=ORIENTED_EDGE('',*,*,#2902,.T.);
#3850=ORIENTED_EDGE('',*,*,#2903,.T.);
#3851=ORIENTED_EDGE('',*,*,#2904,.F.);
#3852=ORIENTED_EDGE('',*,*,#2905,.F.);
#3853=ORIENTED_EDGE('',*,*,#2906,.T.);
#3854=ORIENTED_EDGE('',*,*,#2907,.T.);
#3855=ORIENTED_EDGE('',*,*,#2902,.F.);
#3856=ORIENTED_EDGE('',*,*,#2908,.F.);
#3857=ORIENTED_EDGE('',*,*,#2909,.T.);
#3858=ORIENTED_EDGE('',*,*,#2910,.T.);
#3859=ORIENTED_EDGE('',*,*,#2906,.F.);
#3860=ORIENTED_EDGE('',*,*,#2911,.F.);
#3861=ORIENTED_EDGE('',*,*,#2912,.T.);
#3862=ORIENTED_EDGE('',*,*,#2913,.T.);
#3863=ORIENTED_EDGE('',*,*,#2909,.F.);
#3864=ORIENTED_EDGE('',*,*,#2914,.F.);
#3865=ORIENTED_EDGE('',*,*,#2915,.T.);
#3866=ORIENTED_EDGE('',*,*,#2916,.T.);
#3867=ORIENTED_EDGE('',*,*,#2912,.F.);
#3868=ORIENTED_EDGE('',*,*,#2917,.F.);
#3869=ORIENTED_EDGE('',*,*,#2904,.T.);
#3870=ORIENTED_EDGE('',*,*,#2918,.T.);
#3871=ORIENTED_EDGE('',*,*,#2915,.F.);
#3872=ORIENTED_EDGE('',*,*,#2918,.F.);
#3873=ORIENTED_EDGE('',*,*,#2903,.F.);
#3874=ORIENTED_EDGE('',*,*,#2907,.F.);
#3875=ORIENTED_EDGE('',*,*,#2910,.F.);
#3876=ORIENTED_EDGE('',*,*,#2913,.F.);
#3877=ORIENTED_EDGE('',*,*,#2916,.F.);
#3878=ORIENTED_EDGE('',*,*,#2919,.F.);
#3879=ORIENTED_EDGE('',*,*,#2901,.T.);
#3880=ORIENTED_EDGE('',*,*,#2917,.T.);
#3881=ORIENTED_EDGE('',*,*,#2914,.T.);
#3882=ORIENTED_EDGE('',*,*,#2911,.T.);
#3883=ORIENTED_EDGE('',*,*,#2908,.T.);
#3884=ORIENTED_EDGE('',*,*,#2905,.T.);
#3885=ORIENTED_EDGE('',*,*,#2920,.F.);
#3886=ORIENTED_EDGE('',*,*,#2921,.T.);
#3887=ORIENTED_EDGE('',*,*,#2919,.T.);
#3888=ORIENTED_EDGE('',*,*,#2921,.F.);
#3889=ORIENTED_EDGE('',*,*,#2900,.T.);
#3890=ORIENTED_EDGE('',*,*,#2922,.T.);
#3891=ORIENTED_EDGE('',*,*,#2920,.T.);
#3892=ORIENTED_EDGE('',*,*,#2922,.F.);
#4393=CYLINDRICAL_SURFACE('',#5391,0.1954);
#4590=ADVANCED_FACE('',(#825),#601,.F.);
#4591=ADVANCED_FACE('',(#826),#602,.F.);
#4592=ADVANCED_FACE('',(#827),#603,.F.);
#4593=ADVANCED_FACE('',(#828),#604,.F.);
#4594=ADVANCED_FACE('',(#829),#605,.F.);
#4595=ADVANCED_FACE('',(#830),#606,.F.);
#4596=ADVANCED_FACE('',(#831),#607,.F.);
#4597=ADVANCED_FACE('',(#832),#608,.F.);
#4598=ADVANCED_FACE('',(#833,#499),#609,.T.);
#4599=ADVANCED_FACE('',(#834),#32,.T.);
#4600=ADVANCED_FACE('',(#835),#4393,.T.);
#4719=CLOSED_SHELL('',(#4590,#4591,#4592,#4593,#4594,#4595,#4596,#4597,
#4598,#4599,#4600));
#5377=AXIS2_PLACEMENT_3D('',#10062,#6543,#6544);
#5378=AXIS2_PLACEMENT_3D('',#10063,#6545,#6546);
#5379=AXIS2_PLACEMENT_3D('',#10065,#6547,#6548);
#5380=AXIS2_PLACEMENT_3D('',#10066,#6549,#6550);
#5381=AXIS2_PLACEMENT_3D('',#10075,#6555,#6556);
#5382=AXIS2_PLACEMENT_3D('',#10081,#6560,#6561);
#5383=AXIS2_PLACEMENT_3D('',#10087,#6565,#6566);
#5384=AXIS2_PLACEMENT_3D('',#10093,#6570,#6571);
#5385=AXIS2_PLACEMENT_3D('',#10099,#6575,#6576);
#5386=AXIS2_PLACEMENT_3D('',#10102,#6579,#6580);
#5387=AXIS2_PLACEMENT_3D('',#10103,#6581,#6582);
#5388=AXIS2_PLACEMENT_3D('',#10105,#6583,#6584);
#5389=AXIS2_PLACEMENT_3D('',#10106,#6585,#6586);
#5390=AXIS2_PLACEMENT_3D('',#10108,#6587,#6588);
#5391=AXIS2_PLACEMENT_3D('',#10110,#6590,#6591);
#6543=DIRECTION('axis',(0.,0.,1.));
#6544=DIRECTION('refdir',(1.,0.,0.));
#6545=DIRECTION('center_axis',(0.,1.,0.));
#6546=DIRECTION('ref_axis',(1.,0.,0.));
#6547=DIRECTION('center_axis',(0.,1.,0.));
#6548=DIRECTION('ref_axis',(1.,0.,0.));
#6549=DIRECTION('center_axis',(0.866025403784439,0.,-0.5));
#6550=DIRECTION('ref_axis',(0.5,0.,0.866025403784439));
#6551=DIRECTION('',(0.5,0.,0.866025403784439));
#6552=DIRECTION('',(0.,-1.,0.));
#6553=DIRECTION('',(0.5,0.,0.866025403784439));
#6554=DIRECTION('',(0.,-1.,0.));
#6555=DIRECTION('center_axis',(1.20185167898973E-16,0.,-1.));
#6556=DIRECTION('ref_axis',(1.,0.,1.20185167898973E-16));
#6557=DIRECTION('',(1.,0.,1.20185167898973E-16));
#6558=DIRECTION('',(0.,-1.,0.));
#6559=DIRECTION('',(1.,0.,1.20185167898973E-16));
#6560=DIRECTION('center_axis',(-0.866025403784439,0.,-0.5));
#6561=DIRECTION('ref_axis',(0.5,0.,-0.866025403784439));
#6562=DIRECTION('',(0.5,0.,-0.866025403784439));
#6563=DIRECTION('',(0.,-1.,0.));
#6564=DIRECTION('',(0.5,0.,-0.866025403784439));
#6565=DIRECTION('center_axis',(-0.866025403784439,0.,0.5));
#6566=DIRECTION('ref_axis',(-0.5,0.,-0.866025403784439));
#6567=DIRECTION('',(-0.5,0.,-0.866025403784439));
#6568=DIRECTION('',(0.,-1.,0.));
#6569=DIRECTION('',(-0.5,0.,-0.866025403784439));
#6570=DIRECTION('center_axis',(-2.40370335797945E-16,0.,1.));
#6571=DIRECTION('ref_axis',(-1.,0.,-2.40370335797945E-16));
#6572=DIRECTION('',(-1.,0.,-2.40370335797945E-16));
#6573=DIRECTION('',(0.,-1.,0.));
#6574=DIRECTION('',(-1.,0.,-2.40370335797945E-16));
#6575=DIRECTION('center_axis',(0.866025403784439,0.,0.5));
#6576=DIRECTION('ref_axis',(-0.5,0.,0.866025403784439));
#6577=DIRECTION('',(-0.5,0.,0.866025403784439));
#6578=DIRECTION('',(-0.5,0.,0.866025403784439));
#6579=DIRECTION('center_axis',(0.,-1.,0.));
#6580=DIRECTION('ref_axis',(0.,0.,-1.));
#6581=DIRECTION('center_axis',(0.,1.,0.));
#6582=DIRECTION('ref_axis',(0.,0.,1.));
#6583=DIRECTION('center_axis',(0.,-1.,0.));
#6584=DIRECTION('ref_axis',(1.,0.,0.));
#6585=DIRECTION('center_axis',(0.,-1.,0.));
#6586=DIRECTION('ref_axis',(1.,0.,0.));
#6587=DIRECTION('center_axis',(0.,-1.,0.));
#6588=DIRECTION('ref_axis',(1.,0.,0.));
#6589=DIRECTION('',(0.707106781186548,0.707106781186547,8.65956056235494E-17));
#6590=DIRECTION('center_axis',(0.,-1.,0.));
#6591=DIRECTION('ref_axis',(1.,0.,0.));
#6592=DIRECTION('',(0.,1.,0.));
#10062=CARTESIAN_POINT('',(0.,0.,0.));
#10063=CARTESIAN_POINT('Origin',(0.,-0.4,0.));
#10064=CARTESIAN_POINT('',(-0.1954,-0.4,2.39295984553393E-17));
#10065=CARTESIAN_POINT('Origin',(0.,-0.4,0.));
#10066=CARTESIAN_POINT('Origin',(0.0577350269189626,0.,-0.1));
#10067=CARTESIAN_POINT('',(0.0577350269189626,0.,-0.1));
#10068=CARTESIAN_POINT('',(0.115470053837925,0.,0.));
#10069=CARTESIAN_POINT('',(0.0934187836487032,0.,-0.0381939203391614));
#10070=CARTESIAN_POINT('',(0.0577350269189626,-0.2,-0.1));
#10071=CARTESIAN_POINT('',(0.0577350269189626,0.,-0.1));
#10072=CARTESIAN_POINT('',(0.115470053837925,-0.2,0.));
#10073=CARTESIAN_POINT('',(0.115470053837925,-0.2,0.));
#10074=CARTESIAN_POINT('',(0.115470053837925,0.,0.));
#10075=CARTESIAN_POINT('Origin',(-0.0577350269189626,0.,-0.1));
#10076=CARTESIAN_POINT('',(-0.0577350269189626,0.,-0.1));
#10077=CARTESIAN_POINT('',(0.0561324865405187,0.,-0.1));
#10078=CARTESIAN_POINT('',(-0.0577350269189626,-0.2,-0.1));
#10079=CARTESIAN_POINT('',(-0.0577350269189626,0.,-0.1));
#10080=CARTESIAN_POINT('',(0.0577350269189626,-0.2,-0.1));
#10081=CARTESIAN_POINT('Origin',(-0.115470053837925,0.,-1.38777878078145E-17));
#10082=CARTESIAN_POINT('',(-0.115470053837925,0.,-1.41410031829988E-17));
#10083=CARTESIAN_POINT('',(-0.0797862971081845,0.,-0.0618060796608387));
#10084=CARTESIAN_POINT('',(-0.115470053837925,-0.2,-1.38777878078145E-17));
#10085=CARTESIAN_POINT('',(-0.115470053837925,0.,-1.41410031829988E-17));
#10086=CARTESIAN_POINT('',(-0.0577350269189626,-0.2,-0.1));
#10087=CARTESIAN_POINT('Origin',(-0.0577350269189626,0.,0.1));
#10088=CARTESIAN_POINT('',(-0.0577350269189626,0.,0.1));
#10089=CARTESIAN_POINT('',(-0.0509187836487033,0.,0.111806079660839));
#10090=CARTESIAN_POINT('',(-0.0577350269189626,-0.2,0.1));
#10091=CARTESIAN_POINT('',(-0.0577350269189626,0.,0.1));
#10092=CARTESIAN_POINT('',(-0.115470053837925,-0.2,-1.41410031829988E-17));
#10093=CARTESIAN_POINT('Origin',(0.0577350269189626,0.,0.1));
#10094=CARTESIAN_POINT('',(0.0577350269189626,0.,0.1));
#10095=CARTESIAN_POINT('',(0.113867513459481,0.,0.1));
#10096=CARTESIAN_POINT('',(0.0577350269189626,-0.2,0.1));
#10097=CARTESIAN_POINT('',(0.0577350269189626,0.,0.1));
#10098=CARTESIAN_POINT('',(-0.0577350269189626,-0.2,0.1));
#10099=CARTESIAN_POINT('Origin',(0.115470053837925,0.,0.));
#10100=CARTESIAN_POINT('',(0.122286297108185,0.,-0.0118060796608386));
#10101=CARTESIAN_POINT('',(0.0577350269189626,-0.2,0.1));
#10102=CARTESIAN_POINT('Origin',(0.,-0.2,0.));
#10103=CARTESIAN_POINT('Origin',(0.17,0.,0.));
#10104=CARTESIAN_POINT('',(-0.17,-8.67361737988404E-18,-2.0818995585505E-17));
#10105=CARTESIAN_POINT('Origin',(0.,0.,0.));
#10106=CARTESIAN_POINT('Origin',(0.,-0.015,0.));
#10107=CARTESIAN_POINT('',(-0.1954,-0.0254,-2.39295984553393E-17));
#10108=CARTESIAN_POINT('Origin',(0.,-0.0254,0.));
#10109=CARTESIAN_POINT('',(-0.185,-0.015,-2.2655965784226E-17));
#10110=CARTESIAN_POINT('Origin',(0.,-0.2775,0.));
#10111=CARTESIAN_POINT('',(-0.1954,-0.2775,-2.39295984553393E-17));
#10987=UNCERTAINTY_MEASURE_WITH_UNIT(LENGTH_MEASURE(0.001),#11036,
'DISTANCE_ACCURACY_VALUE',
'Maximum model space distance between geometric entities at asserted c
onnectivities');
#11002=UNCERTAINTY_MEASURE_WITH_UNIT(LENGTH_MEASURE(0.001),#11036,
'DISTANCE_ACCURACY_VALUE',
'Maximum model space distance between geometric entities at asserted c
onnectivities');
#11020=(
GEOMETRIC_REPRESENTATION_CONTEXT(3)
GLOBAL_UNCERTAINTY_ASSIGNED_CONTEXT((#10987))
GLOBAL_UNIT_ASSIGNED_CONTEXT((#11036,#11038,#11039))
REPRESENTATION_CONTEXT('','3D')
);
#11035=(
GEOMETRIC_REPRESENTATION_CONTEXT(3)
GLOBAL_UNCERTAINTY_ASSIGNED_CONTEXT((#11002))
GLOBAL_UNIT_ASSIGNED_CONTEXT((#11036,#11038,#11039))
REPRESENTATION_CONTEXT('','3D')
);
#11036=(
LENGTH_UNIT()
NAMED_UNIT(*)
SI_UNIT(.CENTI.,.METRE.)
);
#11038=(
NAMED_UNIT(*)
PLANE_ANGLE_UNIT()
SI_UNIT($,.RADIAN.)
);
#11039=(
NAMED_UNIT(*)
SI_UNIT($,.STERADIAN.)
SOLID_ANGLE_UNIT()
);
#11057=SHAPE_DEFINITION_REPRESENTATION(#11091,#11170);
#11091=PRODUCT_DEFINITION_SHAPE('',$,#11203);
#11170=SHAPE_REPRESENTATION('',(#5377),#11020);
#11185=PRODUCT_DEFINITION_CONTEXT('part definition',#11283,'design');
#11203=PRODUCT_DEFINITION('M4x4 collar screw','M4x4 collar screw',#11235,
#11185);
#11235=PRODUCT_DEFINITION_FORMATION('',$,#11302);
#11283=APPLICATION_CONTEXT(
'Core Data for Automotive Mechanical Design Process');
#11284=PRODUCT_CONTEXT('part definition',#11283,'mechanical');
#11302=PRODUCT('M4x4 collar screw','M4x4 collar screw',
'M4x4 collar screw',(#11284));
#11387=COLOUR_RGB('Black',0.12,0.14,0.17);
#11388=FILL_AREA_STYLE_COLOUR('',#11387);
#11389=FILL_AREA_STYLE('',(#11388));
#11390=SURFACE_STYLE_FILL_AREA(#11389);
#11391=SURFACE_SIDE_STYLE('',(#11390));
#11392=SURFACE_STYLE_USAGE(.BOTH.,#11391);
#11393=PRESENTATION_STYLE_ASSIGNMENT((#11392));
ENDSEC;
END-ISO-10303-21;
